ISO-10303-21;
HEADER;
/* Generated by software containing ST-Developer
 * from STEP Tools, Inc. (www.steptools.com) 
 */

FILE_DESCRIPTION(
/* description */ (''),
/* implementation_level */ '2;1');

FILE_NAME(
/* name */ 'M5x14 Cap Screw.step',
/* time_stamp */ '2026-10-29T16:43:51-07:00',
/* author */ (''),
/* organization */ (''),
/* preprocessor_version */ 'ST-DEVELOPER v20.2',
/* originating_system */ 'Autodesk Translation Framework v15.17.0.0',
/* authorisation */ '');

FILE_SCHEMA (('AUTOMOTIVE_DESIGN { 1 0 10303 214 3 1 1 }'));
ENDSEC;

DATA;
#10=MECHANICAL_DESIGN_GEOMETRIC_PRESENTATION_REPRESENTATION('',(#368),#10292);
#283=ORIENTED_CLOSED_SHELL('',*,#5010,.F.);
#288=BREP_WITH_VOIDS('Body1',#5011,(#283));
#295=CONICAL_SURFACE('',#5407,0.4,0.785398163397448);
#296=CONICAL_SURFACE('',#5411,0.41,0.785398163397448);
#297=CONICAL_SURFACE('',#5415,0.26,0.463647609000806);
#322=SHAPE_REPRESENTATION_RELATIONSHIP('SRR','None',#10418,#345);
#345=ADVANCED_BREP_SHAPE_REPRESENTATION('',(#288),#10270);
#368=STYLED_ITEM('',(#10635),#288);
#448=FACE_BOUND('',#1104,.T.);
#555=PLANE('',#5395);
#556=PLANE('',#5396);
#557=PLANE('',#5397);
#558=PLANE('',#5398);
#559=PLANE('',#5399);
#560=PLANE('',#5400);
#561=PLANE('',#5401);
#562=PLANE('',#5402);
#563=PLANE('',#5403);
#564=PLANE('',#5405);
#565=PLANE('',#5413);
#760=FACE_OUTER_BOUND('',#1090,.T.);
#761=FACE_OUTER_BOUND('',#1091,.T.);
#762=FACE_OUTER_BOUND('',#1092,.T.);
#763=FACE_OUTER_BOUND('',#1093,.T.);
#764=FACE_OUTER_BOUND('',#1094,.T.);
#765=FACE_OUTER_BOUND('',#1095,.T.);
#766=FACE_OUTER_BOUND('',#1096,.T.);
#767=FACE_OUTER_BOUND('',#1097,.T.);
#768=FACE_OUTER_BOUND('',#1098,.T.);
#769=FACE_OUTER_BOUND('',#1099,.T.);
#770=FACE_OUTER_BOUND('',#1100,.T.);
#771=FACE_OUTER_BOUND('',#1101,.T.);
#772=FACE_OUTER_BOUND('',#1102,.T.);
#773=FACE_OUTER_BOUND('',#1103,.T.);
#774=FACE_OUTER_BOUND('',#1105,.T.);
#775=FACE_OUTER_BOUND('',#1106,.T.);
#1090=EDGE_LOOP('',(#3669,#3670,#3671,#3672));
#1091=EDGE_LOOP('',(#3673,#3674,#3675,#3676));
#1092=EDGE_LOOP('',(#3677,#3678,#3679,#3680));
#1093=EDGE_LOOP('',(#3681,#3682,#3683,#3684));
#1094=EDGE_LOOP('',(#3685,#3686,#3687,#3688));
#1095=EDGE_LOOP('',(#3689,#3690,#3691,#3692));
#1096=EDGE_LOOP('',(#3693,#3694,#3695,#3696,#3697,#3698));
#1097=EDGE_LOOP('',(#3699,#3700,#3701,#3702,#3703,#3704));
#1098=EDGE_LOOP('',(#3705));
#1099=EDGE_LOOP('',(#3706));
#1100=EDGE_LOOP('',(#3707,#3708,#3709,#3710));
#1101=EDGE_LOOP('',(#3711,#3712,#3713,#3714));
#1102=EDGE_LOOP('',(#3715,#3716,#3717,#3718));
#1103=EDGE_LOOP('',(#3719));
#1104=EDGE_LOOP('',(#3720));
#1105=EDGE_LOOP('',(#3721,#3722,#3723,#3724));
#1106=EDGE_LOOP('',(#3725,#3726,#3727,#3728));
#1491=LINE('',#7681,#1883);
#1492=LINE('',#7683,#1884);
#1493=LINE('',#7685,#1885);
#1494=LINE('',#7686,#1886);
#1495=LINE('',#7689,#1887);
#1496=LINE('',#7691,#1888);
#1497=LINE('',#7692,#1889);
#1498=LINE('',#7695,#1890);
#1499=LINE('',#7697,#1891);
#1500=LINE('',#7698,#1892);
#1501=LINE('',#7701,#1893);
#1502=LINE('',#7703,#1894);
#1503=LINE('',#7704,#1895);
#1504=LINE('',#7707,#1896);
#1505=LINE('',#7709,#1897);
#1506=LINE('',#7710,#1898);
#1507=LINE('',#7712,#1899);
#1508=LINE('',#7713,#1900);
#1509=LINE('',#7725,#1901);
#1510=LINE('',#7729,#1902);
#1511=LINE('',#7733,#1903);
#1512=LINE('',#7740,#1904);
#1513=LINE('',#7742,#1905);
#1883=VECTOR('',#6158,1.);
#1884=VECTOR('',#6159,1.);
#1885=VECTOR('',#6160,1.);
#1886=VECTOR('',#6161,1.);
#1887=VECTOR('',#6164,1.);
#1888=VECTOR('',#6165,1.);
#1889=VECTOR('',#6166,1.);
#1890=VECTOR('',#6169,1.);
#1891=VECTOR('',#6170,1.);
#1892=VECTOR('',#6171,1.);
#1893=VECTOR('',#6174,1.);
#1894=VECTOR('',#6175,1.);
#1895=VECTOR('',#6176,1.);
#1896=VECTOR('',#6179,1.);
#1897=VECTOR('',#6180,1.);
#1898=VECTOR('',#6181,1.);
#1899=VECTOR('',#6184,1.);
#1900=VECTOR('',#6185,1.);
#1901=VECTOR('',#6202,0.4);
#1902=VECTOR('',#6207,0.425);
#1903=VECTOR('',#6212,0.41);
#1904=VECTOR('',#6221,0.26);
#1905=VECTOR('',#6224,0.25);
#2245=CIRCLE('',#5404,0.24505);
#2246=CIRCLE('',#5406,0.375);
#2247=CIRCLE('',#5408,0.425);
#2248=CIRCLE('',#5410,0.425);
#2249=CIRCLE('',#5412,0.395);
#2250=CIRCLE('',#5414,0.27);
#2251=CIRCLE('',#5416,0.24505);
#2480=VERTEX_POINT('',#7679);
#2481=VERTEX_POINT('',#7680);
#2482=VERTEX_POINT('',#7682);
#2483=VERTEX_POINT('',#7684);
#2484=VERTEX_POINT('',#7688);
#2485=VERTEX_POINT('',#7690);
#2486=VERTEX_POINT('',#7694);
#2487=VERTEX_POINT('',#7696);
#2488=VERTEX_POINT('',#7700);
#2489=VERTEX_POINT('',#7702);
#2490=VERTEX_POINT('',#7706);
#2491=VERTEX_POINT('',#7708);
#2492=VERTEX_POINT('',#7717);
#2493=VERTEX_POINT('',#7720);
#2494=VERTEX_POINT('',#7723);
#2495=VERTEX_POINT('',#7727);
#2496=VERTEX_POINT('',#7731);
#2497=VERTEX_POINT('',#7735);
#2498=VERTEX_POINT('',#7738);
#2925=EDGE_CURVE('',#2480,#2481,#1491,.T.);
#2926=EDGE_CURVE('',#2481,#2482,#1492,.T.);
#2927=EDGE_CURVE('',#2482,#2483,#1493,.T.);
#2928=EDGE_CURVE('',#2480,#2483,#1494,.T.);
#2929=EDGE_CURVE('',#2481,#2484,#1495,.T.);
#2930=EDGE_CURVE('',#2484,#2485,#1496,.T.);
#2931=EDGE_CURVE('',#2485,#2482,#1497,.T.);
#2932=EDGE_CURVE('',#2484,#2486,#1498,.T.);
#2933=EDGE_CURVE('',#2486,#2487,#1499,.T.);
#2934=EDGE_CURVE('',#2487,#2485,#1500,.T.);
#2935=EDGE_CURVE('',#2486,#2488,#1501,.T.);
#2936=EDGE_CURVE('',#2488,#2489,#1502,.T.);
#2937=EDGE_CURVE('',#2489,#2487,#1503,.T.);
#2938=EDGE_CURVE('',#2488,#2490,#1504,.T.);
#2939=EDGE_CURVE('',#2490,#2491,#1505,.T.);
#2940=EDGE_CURVE('',#2491,#2489,#1506,.T.);
#2941=EDGE_CURVE('',#2490,#2480,#1507,.T.);
#2942=EDGE_CURVE('',#2483,#2491,#1508,.T.);
#2943=EDGE_CURVE('',#2492,#2492,#2245,.T.);
#2944=EDGE_CURVE('',#2493,#2493,#2246,.T.);
#2945=EDGE_CURVE('',#2494,#2494,#2247,.T.);
#2946=EDGE_CURVE('',#2494,#2493,#1509,.T.);
#2947=EDGE_CURVE('',#2495,#2495,#2248,.T.);
#2948=EDGE_CURVE('',#2495,#2494,#1510,.T.);
#2949=EDGE_CURVE('',#2496,#2496,#2249,.T.);
#2950=EDGE_CURVE('',#2496,#2495,#1511,.T.);
#2951=EDGE_CURVE('',#2497,#2497,#2250,.T.);
#2952=EDGE_CURVE('',#2498,#2498,#2251,.F.);
#2953=EDGE_CURVE('',#2498,#2497,#1512,.T.);
#2954=EDGE_CURVE('',#2492,#2498,#1513,.T.);
#3669=ORIENTED_EDGE('',*,*,#2925,.T.);
#3670=ORIENTED_EDGE('',*,*,#2926,.T.);
#3671=ORIENTED_EDGE('',*,*,#2927,.T.);
#3672=ORIENTED_EDGE('',*,*,#2928,.F.);
#3673=ORIENTED_EDGE('',*,*,#2929,.T.);
#3674=ORIENTED_EDGE('',*,*,#2930,.T.);
#3675=ORIENTED_EDGE('',*,*,#2931,.T.);
#3676=ORIENTED_EDGE('',*,*,#2926,.F.);
#3677=ORIENTED_EDGE('',*,*,#2932,.T.);
#3678=ORIENTED_EDGE('',*,*,#2933,.T.);
#3679=ORIENTED_EDGE('',*,*,#2934,.T.);
#3680=ORIENTED_EDGE('',*,*,#2930,.F.);
#3681=ORIENTED_EDGE('',*,*,#2935,.T.);
#3682=ORIENTED_EDGE('',*,*,#2936,.T.);
#3683=ORIENTED_EDGE('',*,*,#2937,.T.);
#3684=ORIENTED_EDGE('',*,*,#2933,.F.);
#3685=ORIENTED_EDGE('',*,*,#2938,.T.);
#3686=ORIENTED_EDGE('',*,*,#2939,.T.);
#3687=ORIENTED_EDGE('',*,*,#2940,.T.);
#3688=ORIENTED_EDGE('',*,*,#2936,.F.);
#3689=ORIENTED_EDGE('',*,*,#2941,.T.);
#3690=ORIENTED_EDGE('',*,*,#2928,.T.);
#3691=ORIENTED_EDGE('',*,*,#2942,.T.);
#3692=ORIENTED_EDGE('',*,*,#2939,.F.);
#3693=ORIENTED_EDGE('',*,*,#2941,.F.);
#3694=ORIENTED_EDGE('',*,*,#2938,.F.);
#3695=ORIENTED_EDGE('',*,*,#2935,.F.);
#3696=ORIENTED_EDGE('',*,*,#2932,.F.);
#3697=ORIENTED_EDGE('',*,*,#2929,.F.);
#3698=ORIENTED_EDGE('',*,*,#2925,.F.);
#3699=ORIENTED_EDGE('',*,*,#2942,.F.);
#3700=ORIENTED_EDGE('',*,*,#2927,.F.);
#3701=ORIENTED_EDGE('',*,*,#2931,.F.);
#3702=ORIENTED_EDGE('',*,*,#2934,.F.);
#3703=ORIENTED_EDGE('',*,*,#2937,.F.);
#3704=ORIENTED_EDGE('',*,*,#2940,.F.);
#3705=ORIENTED_EDGE('',*,*,#2943,.F.);
#3706=ORIENTED_EDGE('',*,*,#2944,.F.);
#3707=ORIENTED_EDGE('',*,*,#2945,.F.);
#3708=ORIENTED_EDGE('',*,*,#2946,.T.);
#3709=ORIENTED_EDGE('',*,*,#2944,.T.);
#3710=ORIENTED_EDGE('',*,*,#2946,.F.);
#3711=ORIENTED_EDGE('',*,*,#2947,.F.);
#3712=ORIENTED_EDGE('',*,*,#2948,.T.);
#3713=ORIENTED_EDGE('',*,*,#2945,.T.);
#3714=ORIENTED_EDGE('',*,*,#2948,.F.);
#3715=ORIENTED_EDGE('',*,*,#2949,.F.);
#3716=ORIENTED_EDGE('',*,*,#2950,.T.);
#3717=ORIENTED_EDGE('',*,*,#2947,.T.);
#3718=ORIENTED_EDGE('',*,*,#2950,.F.);
#3719=ORIENTED_EDGE('',*,*,#2949,.T.);
#3720=ORIENTED_EDGE('',*,*,#2951,.F.);
#3721=ORIENTED_EDGE('',*,*,#2952,.F.);
#3722=ORIENTED_EDGE('',*,*,#2953,.T.);
#3723=ORIENTED_EDGE('',*,*,#2951,.T.);
#3724=ORIENTED_EDGE('',*,*,#2953,.F.);
#3725=ORIENTED_EDGE('',*,*,#2943,.T.);
#3726=ORIENTED_EDGE('',*,*,#2954,.T.);
#3727=ORIENTED_EDGE('',*,*,#2952,.T.);
#3728=ORIENTED_EDGE('',*,*,#2954,.F.);
#4661=CYLINDRICAL_SURFACE('',#5409,0.425);
#4662=CYLINDRICAL_SURFACE('',#5417,0.24505);
#4769=ADVANCED_FACE('',(#760),#555,.F.);
#4770=ADVANCED_FACE('',(#761),#556,.F.);
#4771=ADVANCED_FACE('',(#762),#557,.F.);
#4772=ADVANCED_FACE('',(#763),#558,.F.);
#4773=ADVANCED_FACE('',(#764),#559,.F.);
#4774=ADVANCED_FACE('',(#765),#560,.F.);
#4775=ADVANCED_FACE('',(#766),#561,.F.);
#4776=ADVANCED_FACE('',(#767),#562,.F.);
#4777=ADVANCED_FACE('',(#768),#563,.F.);
#4778=ADVANCED_FACE('',(#769),#564,.T.);
#4779=ADVANCED_FACE('',(#770),#295,.T.);
#4780=ADVANCED_FACE('',(#771),#4661,.T.);
#4781=ADVANCED_FACE('',(#772),#296,.T.);
#4782=ADVANCED_FACE('',(#773,#448),#565,.T.);
#4783=ADVANCED_FACE('',(#774),#297,.T.);
#4784=ADVANCED_FACE('',(#775),#4662,.T.);
#5010=CLOSED_SHELL('',(#4769,#4770,#4771,#4772,#4773,#4774,#4775,#4776));
#5011=CLOSED_SHELL('',(#4777,#4778,#4779,#4780,#4781,#4782,#4783,#4784));
#5394=AXIS2_PLACEMENT_3D('',#7677,#6154,#6155);
#5395=AXIS2_PLACEMENT_3D('',#7678,#6156,#6157);
#5396=AXIS2_PLACEMENT_3D('',#7687,#6162,#6163);
#5397=AXIS2_PLACEMENT_3D('',#7693,#6167,#6168);
#5398=AXIS2_PLACEMENT_3D('',#7699,#6172,#6173);
#5399=AXIS2_PLACEMENT_3D('',#7705,#6177,#6178);
#5400=AXIS2_PLACEMENT_3D('',#7711,#6182,#6183);
#5401=AXIS2_PLACEMENT_3D('',#7714,#6186,#6187);
#5402=AXIS2_PLACEMENT_3D('',#7715,#6188,#6189);
#5403=AXIS2_PLACEMENT_3D('',#7716,#6190,#6191);
#5404=AXIS2_PLACEMENT_3D('',#7718,#6192,#6193);
#5405=AXIS2_PLACEMENT_3D('',#7719,#6194,#6195);
#5406=AXIS2_PLACEMENT_3D('',#7721,#6196,#6197);
#5407=AXIS2_PLACEMENT_3D('',#7722,#6198,#6199);
#5408=AXIS2_PLACEMENT_3D('',#7724,#6200,#6201);
#5409=AXIS2_PLACEMENT_3D('',#7726,#6203,#6204);
#5410=AXIS2_PLACEMENT_3D('',#7728,#6205,#6206);
#5411=AXIS2_PLACEMENT_3D('',#7730,#6208,#6209);
#5412=AXIS2_PLACEMENT_3D('',#7732,#6210,#6211);
#5413=AXIS2_PLACEMENT_3D('',#7734,#6213,#6214);
#5414=AXIS2_PLACEMENT_3D('',#7736,#6215,#6216);
#5415=AXIS2_PLACEMENT_3D('',#7737,#6217,#6218);
#5416=AXIS2_PLACEMENT_3D('',#7739,#6219,#6220);
#5417=AXIS2_PLACEMENT_3D('',#7741,#6222,#6223);
#6154=DIRECTION('axis',(0.,0.,1.));
#6155=DIRECTION('refdir',(1.,0.,0.));
#6156=DIRECTION('center_axis',(0.866025403784439,0.,-0.5));
#6157=DIRECTION('ref_axis',(0.5,0.,0.866025403784439));
#6158=DIRECTION('',(-0.5,0.,-0.866025403784439));
#6159=DIRECTION('',(0.,-1.,0.));
#6160=DIRECTION('',(0.5,0.,0.866025403784439));
#6161=DIRECTION('',(0.,-1.,0.));
#6162=DIRECTION('center_axis',(1.20185167898973E-16,0.,-1.));
#6163=DIRECTION('ref_axis',(1.,0.,1.20185167898973E-16));
#6164=DIRECTION('',(-1.,0.,-1.20185167898973E-16));
#6165=DIRECTION('',(0.,-1.,0.));
#6166=DIRECTION('',(1.,0.,1.20185167898973E-16));
#6167=DIRECTION('center_axis',(-0.866025403784439,0.,-0.5));
#6168=DIRECTION('ref_axis',(0.5,0.,-0.866025403784439));
#6169=DIRECTION('',(-0.5,0.,0.866025403784439));
#6170=DIRECTION('',(0.,-1.,0.));
#6171=DIRECTION('',(0.5,0.,-0.866025403784439));
#6172=DIRECTION('center_axis',(-0.866025403784439,0.,0.5));
#6173=DIRECTION('ref_axis',(-0.5,0.,-0.866025403784439));
#6174=DIRECTION('',(0.5,0.,0.866025403784439));
#6175=DIRECTION('',(0.,-1.,0.));
#6176=DIRECTION('',(-0.5,0.,-0.866025403784439));
#6177=DIRECTION('center_axis',(-2.40370335797945E-16,0.,1.));
#6178=DIRECTION('ref_axis',(-1.,0.,-2.40370335797945E-16));
#6179=DIRECTION('',(1.,0.,2.40370335797945E-16));
#6180=DIRECTION('',(0.,-1.,0.));
#6181=DIRECTION('',(-1.,0.,-2.40370335797945E-16));
#6182=DIRECTION('center_axis',(0.866025403784439,0.,0.5));
#6183=DIRECTION('ref_axis',(-0.5,0.,0.866025403784439));
#6184=DIRECTION('',(0.5,0.,-0.866025403784439));
#6185=DIRECTION('',(-0.5,0.,0.866025403784439));
#6186=DIRECTION('center_axis',(0.,1.,0.));
#6187=DIRECTION('ref_axis',(1.,0.,0.));
#6188=DIRECTION('center_axis',(0.,-1.,0.));
#6189=DIRECTION('ref_axis',(0.,0.,-1.));
#6190=DIRECTION('center_axis',(0.,1.,0.));
#6191=DIRECTION('ref_axis',(1.,0.,0.));
#6192=DIRECTION('center_axis',(0.,1.,0.));
#6193=DIRECTION('ref_axis',(1.,0.,0.));
#6194=DIRECTION('center_axis',(0.,1.,0.));
#6195=DIRECTION('ref_axis',(0.,0.,1.));
#6196=DIRECTION('center_axis',(0.,-1.,0.));
#6197=DIRECTION('ref_axis',(1.,0.,0.));
#6198=DIRECTION('center_axis',(0.,-1.,0.));
#6199=DIRECTION('ref_axis',(1.,0.,0.));
#6200=DIRECTION('center_axis',(0.,-1.,0.));
#6201=DIRECTION('ref_axis',(1.,0.,0.));
#6202=DIRECTION('',(0.707106781186548,0.707106781186547,8.65956056235493E-17));
#6203=DIRECTION('center_axis',(0.,-1.,0.));
#6204=DIRECTION('ref_axis',(1.,0.,0.));
#6205=DIRECTION('center_axis',(0.,-1.,0.));
#6206=DIRECTION('ref_axis',(1.,0.,0.));
#6207=DIRECTION('',(0.,1.,0.));
#6208=DIRECTION('center_axis',(0.,1.,0.));
#6209=DIRECTION('ref_axis',(1.,0.,0.));
#6210=DIRECTION('center_axis',(0.,-1.,0.));
#6211=DIRECTION('ref_axis',(1.,0.,0.));
#6212=DIRECTION('',(-0.707106781186547,0.707106781186548,-8.65956056235493E-17));
#6213=DIRECTION('center_axis',(0.,-1.,0.));
#6214=DIRECTION('ref_axis',(0.,0.,-1.));
#6215=DIRECTION('center_axis',(0.,-1.,0.));
#6216=DIRECTION('ref_axis',(1.,0.,0.));
#6217=DIRECTION('center_axis',(0.,1.,0.));
#6218=DIRECTION('ref_axis',(1.,0.,0.));
#6219=DIRECTION('center_axis',(0.,1.,0.));
#6220=DIRECTION('ref_axis',(1.,0.,0.));
#6221=DIRECTION('',(-0.447213595499958,0.894427190999916,-5.47678698264203E-17));
#6222=DIRECTION('center_axis',(0.,-1.,0.));
#6223=DIRECTION('ref_axis',(1.,0.,0.));
#6224=DIRECTION('',(0.,1.,0.));
#7677=CARTESIAN_POINT('',(0.,0.,0.));
#7678=CARTESIAN_POINT('Origin',(0.115470053837925,-0.5,-0.2));
#7679=CARTESIAN_POINT('',(0.23094010767585,-0.5,0.));
#7680=CARTESIAN_POINT('',(0.115470053837925,-0.5,-0.2));
#7681=CARTESIAN_POINT('',(0.23094010767585,-0.5,0.));
#7682=CARTESIAN_POINT('',(0.115470053837925,-0.8,-0.2));
#7683=CARTESIAN_POINT('',(0.115470053837925,-0.5,-0.2));
#7684=CARTESIAN_POINT('',(0.23094010767585,-0.8,0.));
#7685=CARTESIAN_POINT('',(0.23094010767585,-0.8,0.));
#7686=CARTESIAN_POINT('',(0.23094010767585,-0.5,0.));
#7687=CARTESIAN_POINT('Origin',(-0.115470053837925,-0.5,-0.2));
#7688=CARTESIAN_POINT('',(-0.115470053837925,-0.5,-0.2));
#7689=CARTESIAN_POINT('',(0.115470053837925,-0.5,-0.2));
#7690=CARTESIAN_POINT('',(-0.115470053837925,-0.8,-0.2));
#7691=CARTESIAN_POINT('',(-0.115470053837925,-0.5,-0.2));
#7692=CARTESIAN_POINT('',(0.115470053837925,-0.8,-0.2));
#7693=CARTESIAN_POINT('Origin',(-0.23094010767585,-0.5,-2.77555756156289E-17));
#7694=CARTESIAN_POINT('',(-0.23094010767585,-0.5,-2.82820063659975E-17));
#7695=CARTESIAN_POINT('',(-0.115470053837925,-0.5,-0.2));
#7696=CARTESIAN_POINT('',(-0.23094010767585,-0.8,-2.77555756156289E-17));
#7697=CARTESIAN_POINT('',(-0.23094010767585,-0.5,-2.82820063659975E-17));
#7698=CARTESIAN_POINT('',(-0.115470053837925,-0.8,-0.2));
#7699=CARTESIAN_POINT('Origin',(-0.115470053837925,-0.5,0.2));
#7700=CARTESIAN_POINT('',(-0.115470053837925,-0.5,0.2));
#7701=CARTESIAN_POINT('',(-0.23094010767585,-0.5,-2.82820063659975E-17));
#7702=CARTESIAN_POINT('',(-0.115470053837925,-0.8,0.2));
#7703=CARTESIAN_POINT('',(-0.115470053837925,-0.5,0.2));
#7704=CARTESIAN_POINT('',(-0.23094010767585,-0.8,-2.82820063659975E-17));
#7705=CARTESIAN_POINT('Origin',(0.115470053837925,-0.5,0.2));
#7706=CARTESIAN_POINT('',(0.115470053837925,-0.5,0.2));
#7707=CARTESIAN_POINT('',(-0.115470053837925,-0.5,0.2));
#7708=CARTESIAN_POINT('',(0.115470053837925,-0.8,0.2));
#7709=CARTESIAN_POINT('',(0.115470053837925,-0.5,0.2));
#7710=CARTESIAN_POINT('',(-0.115470053837925,-0.8,0.2));
#7711=CARTESIAN_POINT('Origin',(0.23094010767585,-0.5,0.));
#7712=CARTESIAN_POINT('',(0.115470053837925,-0.5,0.2));
#7713=CARTESIAN_POINT('',(0.115470053837925,-0.8,0.2));
#7714=CARTESIAN_POINT('Origin',(0.,-0.5,0.));
#7715=CARTESIAN_POINT('Origin',(0.,-0.8,0.));
#7716=CARTESIAN_POINT('Origin',(0.,-1.4,0.));
#7717=CARTESIAN_POINT('',(-0.24505,-1.4,3.00099698131059E-17));
#7718=CARTESIAN_POINT('Origin',(0.,-1.4,0.));
#7719=CARTESIAN_POINT('Origin',(0.375,0.5,0.));
#7720=CARTESIAN_POINT('',(-0.375,0.5,-4.59242549680257E-17));
#7721=CARTESIAN_POINT('Origin',(0.,0.5,0.));
#7722=CARTESIAN_POINT('Origin',(0.,0.475,0.));
#7723=CARTESIAN_POINT('',(-0.425,0.45,-5.20474889637625E-17));
#7724=CARTESIAN_POINT('Origin',(0.,0.45,0.));
#7725=CARTESIAN_POINT('',(-0.4,0.475,-4.89858719658941E-17));
#7726=CARTESIAN_POINT('Origin',(0.,0.24,0.));
#7727=CARTESIAN_POINT('',(-0.425,0.0299999999999998,-5.20474889637625E-17));
#7728=CARTESIAN_POINT('Origin',(0.,0.0299999999999998,0.));
#7729=CARTESIAN_POINT('',(-0.425,0.24,-5.20474889637625E-17));
#7730=CARTESIAN_POINT('Origin',(0.,0.0150000000000001,0.));
#7731=CARTESIAN_POINT('',(-0.395,4.85722573273506E-17,-4.83735485663204E-17));
#7732=CARTESIAN_POINT('Origin',(0.,0.,0.));
#7733=CARTESIAN_POINT('',(-0.41,0.0150000000000001,-5.02105187650415E-17));
#7734=CARTESIAN_POINT('Origin',(0.27,0.,0.));
#7735=CARTESIAN_POINT('',(-0.27,0.,-3.30654635769785E-17));
#7736=CARTESIAN_POINT('Origin',(0.,0.,0.));
#7737=CARTESIAN_POINT('Origin',(0.,-0.02,0.));
#7738=CARTESIAN_POINT('',(-0.24505,-0.0498999999999999,3.00099698131059E-17));
#7739=CARTESIAN_POINT('Origin',(0.,-0.0498999999999999,0.));
#7740=CARTESIAN_POINT('',(-0.26,-0.02,-3.18408167778312E-17));
#7741=CARTESIAN_POINT('Origin',(0.,-0.995,0.));
#7742=CARTESIAN_POINT('',(-0.24505,-0.995,-3.00099698131059E-17));
#10242=UNCERTAINTY_MEASURE_WITH_UNIT(LENGTH_MEASURE(0.001),#10293,
'DISTANCE_ACCURACY_VALUE',
'Maximum model space distance between geometric entities at asserted c
onnectivities');
#10264=UNCERTAINTY_MEASURE_WITH_UNIT(LENGTH_MEASURE(0.001),#10293,
'DISTANCE_ACCURACY_VALUE',
'Maximum model space distance between geometric entities at asserted c
onnectivities');
#10270=(
GEOMETRIC_REPRESENTATION_CONTEXT(3)
GLOBAL_UNCERTAINTY_ASSIGNED_CONTEXT((#10242))
GLOBAL_UNIT_ASSIGNED_CONTEXT((#10293,#10295,#10296))
REPRESENTATION_CONTEXT('','3D')
);
#10292=(
GEOMETRIC_REPRESENTATION_CONTEXT(3)
GLOBAL_UNCERTAINTY_ASSIGNED_CONTEXT((#10264))
GLOBAL_UNIT_ASSIGNED_CONTEXT((#10293,#10295,#10296))
REPRESENTATION_CONTEXT('','3D')
);
#10293=(
LENGTH_UNIT()
NAMED_UNIT(*)
SI_UNIT(.CENTI.,.METRE.)
);
#10295=(
NAMED_UNIT(*)
PLANE_ANGLE_UNIT()
SI_UNIT($,.RADIAN.)
);
#10296=(
NAMED_UNIT(*)
SI_UNIT($,.STERADIAN.)
SOLID_ANGLE_UNIT()
);
#10302=SHAPE_DEFINITION_REPRESENTATION(#10329,#10418);
#10329=PRODUCT_DEFINITION_SHAPE('',$,#10446);
#10418=SHAPE_REPRESENTATION('',(#5394),#10270);
#10440=PRODUCT_DEFINITION_CONTEXT('part definition',#10523,'design');
#10446=PRODUCT_DEFINITION('M5x14 Cap Screw','M5x14 Cap Screw',#10473,
#10440);
#10473=PRODUCT_DEFINITION_FORMATION('',$,#10530);
#10523=APPLICATION_CONTEXT(
'Core Data for Automotive Mechanical Design Process');
#10524=PRODUCT_CONTEXT('part definition',#10523,'mechanical');
#10530=PRODUCT('M5x14 Cap Screw','M5x14 Cap Screw',
'M5x14 Cap Screw',(#10524));
#10629=COLOUR_RGB('Black',0.12,0.14,0.17);
#10630=FILL_AREA_STYLE_COLOUR('',#10629);
#10631=FILL_AREA_STYLE('',(#10630));
#10632=SURFACE_STYLE_FILL_AREA(#10631);
#10633=SURFACE_SIDE_STYLE('',(#10632));
#10634=SURFACE_STYLE_USAGE(.BOTH.,#10633);
#10635=PRESENTATION_STYLE_ASSIGNMENT((#10634));
ENDSEC;
END-ISO-10303-21;
